ISO-10303-21;
HEADER;
/* Generated by software containing ST-Developer
 * from STEP Tools, Inc. (www.steptools.com) 
 */

FILE_DESCRIPTION(
/* description */ ('Twin-shaft manual slide'),
/* implementation_level */ '2;1');

FILE_NAME(
/* name */ 'Flat Washer - M6.step',
/* time_stamp */ '2026-10-27T18:38:08-07:00',
/* author */ (''),
/* organization */ (''),
/* preprocessor_version */ 'ST-DEVELOPER v20.2',
/* originating_system */ 'Autodesk Translation Framework v15.17.0.0',
/* authorisation */ '');

FILE_SCHEMA (('AUTOMOTIVE_DESIGN { 1 0 10303 214 3 1 1 }'));
ENDSEC;

DATA;
#10=MECHANICAL_DESIGN_GEOMETRIC_PRESENTATION_REPRESENTATION('',(#290),#6463);
#258=SHAPE_REPRESENTATION_RELATIONSHIP('SRR','None',#6578,#274);
#274=ADVANCED_BREP_SHAPE_REPRESENTATION('',(#303),#6461);
#290=STYLED_ITEM('',(#6747),#303);
#303=MANIFOLD_SOLID_BREP('Body1',#3655);
#398=FACE_BOUND('',#1016,.T.);
#399=FACE_BOUND('',#1018,.T.);
#513=PLANE('',#4216);
#514=PLANE('',#4217);
#712=FACE_OUTER_BOUND('',#1013,.T.);
#713=FACE_OUTER_BOUND('',#1014,.T.);
#714=FACE_OUTER_BOUND('',#1015,.T.);
#715=FACE_OUTER_BOUND('',#1017,.T.);
#1013=EDGE_LOOP('',(#3290,#3291,#3292,#3293));
#1014=EDGE_LOOP('',(#3294,#3295,#3296,#3297));
#1015=EDGE_LOOP('',(#3298));
#1016=EDGE_LOOP('',(#3299));
#1017=EDGE_LOOP('',(#3300));
#1018=EDGE_LOOP('',(#3301));
#1297=LINE('',#6319,#1583);
#1298=LINE('',#6325,#1584);
#1583=VECTOR('',#5281,0.32);
#1584=VECTOR('',#5288,0.6);
#1750=CIRCLE('',#4211,0.32);
#1751=CIRCLE('',#4212,0.32);
#1752=CIRCLE('',#4214,0.6);
#1753=CIRCLE('',#4215,0.6);
#2025=VERTEX_POINT('',#6316);
#2026=VERTEX_POINT('',#6318);
#2027=VERTEX_POINT('',#6322);
#2028=VERTEX_POINT('',#6324);
#2450=EDGE_CURVE('',#2025,#2025,#1750,.T.);
#2451=EDGE_CURVE('',#2025,#2026,#1297,.T.);
#2452=EDGE_CURVE('',#2026,#2026,#1751,.T.);
#2453=EDGE_CURVE('',#2027,#2027,#1752,.T.);
#2454=EDGE_CURVE('',#2027,#2028,#1298,.T.);
#2455=EDGE_CURVE('',#2028,#2028,#1753,.T.);
#3290=ORIENTED_EDGE('',*,*,#2450,.F.);
#3291=ORIENTED_EDGE('',*,*,#2451,.T.);
#3292=ORIENTED_EDGE('',*,*,#2452,.T.);
#3293=ORIENTED_EDGE('',*,*,#2451,.F.);
#3294=ORIENTED_EDGE('',*,*,#2453,.F.);
#3295=ORIENTED_EDGE('',*,*,#2454,.T.);
#3296=ORIENTED_EDGE('',*,*,#2455,.T.);
#3297=ORIENTED_EDGE('',*,*,#2454,.F.);
#3298=ORIENTED_EDGE('',*,*,#2453,.T.);
#3299=ORIENTED_EDGE('',*,*,#2450,.T.);
#3300=ORIENTED_EDGE('',*,*,#2455,.F.);
#3301=ORIENTED_EDGE('',*,*,#2452,.F.);
#3427=CYLINDRICAL_SURFACE('',#4210,0.32);
#3428=CYLINDRICAL_SURFACE('',#4213,0.6);
#3617=ADVANCED_FACE('',(#712),#3427,.F.);
#3618=ADVANCED_FACE('',(#713),#3428,.T.);
#3619=ADVANCED_FACE('',(#714,#398),#513,.T.);
#3620=ADVANCED_FACE('',(#715,#399),#514,.F.);
#3655=CLOSED_SHELL('',(#3617,#3618,#3619,#3620));
#4209=AXIS2_PLACEMENT_3D('',#6314,#5275,#5276);
#4210=AXIS2_PLACEMENT_3D('',#6315,#5277,#5278);
#4211=AXIS2_PLACEMENT_3D('',#6317,#5279,#5280);
#4212=AXIS2_PLACEMENT_3D('',#6320,#5282,#5283);
#4213=AXIS2_PLACEMENT_3D('',#6321,#5284,#5285);
#4214=AXIS2_PLACEMENT_3D('',#6323,#5286,#5287);
#4215=AXIS2_PLACEMENT_3D('',#6326,#5289,#5290);
#4216=AXIS2_PLACEMENT_3D('',#6327,#5291,#5292);
#4217=AXIS2_PLACEMENT_3D('',#6328,#5293,#5294);
#5275=DIRECTION('axis',(0.,0.,1.));
#5276=DIRECTION('refdir',(1.,0.,0.));
#5277=DIRECTION('center_axis',(0.,1.,0.));
#5278=DIRECTION('ref_axis',(1.,0.,0.));
#5279=DIRECTION('center_axis',(0.,-1.,0.));
#5280=DIRECTION('ref_axis',(1.,0.,0.));
#5281=DIRECTION('',(0.,-1.,0.));
#5282=DIRECTION('center_axis',(0.,-1.,0.));
#5283=DIRECTION('ref_axis',(1.,0.,0.));
#5284=DIRECTION('center_axis',(0.,1.,0.));
#5285=DIRECTION('ref_axis',(1.,0.,0.));
#5286=DIRECTION('center_axis',(0.,1.,0.));
#5287=DIRECTION('ref_axis',(1.,0.,0.));
#5288=DIRECTION('',(0.,-1.,0.));
#5289=DIRECTION('center_axis',(0.,1.,0.));
#5290=DIRECTION('ref_axis',(1.,0.,0.));
#5291=DIRECTION('center_axis',(0.,1.,0.));
#5292=DIRECTION('ref_axis',(1.,0.,0.));
#5293=DIRECTION('center_axis',(0.,1.,0.));
#5294=DIRECTION('ref_axis',(1.,0.,0.));
#6314=CARTESIAN_POINT('',(0.,0.,0.));
#6315=CARTESIAN_POINT('Origin',(0.,0.,0.));
#6316=CARTESIAN_POINT('',(-0.32,0.16,3.91886975727153E-17));
#6317=CARTESIAN_POINT('Origin',(0.,0.16,0.));
#6318=CARTESIAN_POINT('',(-0.32,0.,3.91886975727153E-17));
#6319=CARTESIAN_POINT('',(-0.32,0.,3.91886975727153E-17));
#6320=CARTESIAN_POINT('Origin',(0.,0.,0.));
#6321=CARTESIAN_POINT('Origin',(0.,0.,0.));
#6322=CARTESIAN_POINT('',(-0.6,0.16,7.34788079488412E-17));
#6323=CARTESIAN_POINT('Origin',(0.,0.16,0.));
#6324=CARTESIAN_POINT('',(-0.6,0.,7.34788079488412E-17));
#6325=CARTESIAN_POINT('',(-0.6,0.,7.34788079488412E-17));
#6326=CARTESIAN_POINT('Origin',(0.,0.,0.));
#6327=CARTESIAN_POINT('Origin',(0.,0.16,0.));
#6328=CARTESIAN_POINT('Origin',(0.,0.,0.));
#6440=UNCERTAINTY_MEASURE_WITH_UNIT(LENGTH_MEASURE(0.001),#6464,
'DISTANCE_ACCURACY_VALUE',
'Maximum model space distance between geometric entities at asserted c
onnectivities');
#6442=UNCERTAINTY_MEASURE_WITH_UNIT(LENGTH_MEASURE(0.001),#6464,
'DISTANCE_ACCURACY_VALUE',
'Maximum model space distance between geometric entities at asserted c
onnectivities');
#6461=(
GEOMETRIC_REPRESENTATION_CONTEXT(3)
GLOBAL_UNCERTAINTY_ASSIGNED_CONTEXT((#6440))
GLOBAL_UNIT_ASSIGNED_CONTEXT((#6464,#6466,#6467))
REPRESENTATION_CONTEXT('','3D')
);
#6463=(
GEOMETRIC_REPRESENTATION_CONTEXT(3)
GLOBAL_UNCERTAINTY_ASSIGNED_CONTEXT((#6442))
GLOBAL_UNIT_ASSIGNED_CONTEXT((#6464,#6466,#6467))
REPRESENTATION_CONTEXT('','3D')
);
#6464=(
LENGTH_UNIT()
NAMED_UNIT(*)
SI_UNIT(.CENTI.,.METRE.)
);
#6466=(
NAMED_UNIT(*)
PLANE_ANGLE_UNIT()
SI_UNIT($,.RADIAN.)
);
#6467=(
NAMED_UNIT(*)
SI_UNIT($,.STERADIAN.)
SOLID_ANGLE_UNIT()
);
#6486=SHAPE_DEFINITION_REPRESENTATION(#6535,#6578);
#6535=PRODUCT_DEFINITION_SHAPE('',$,#6599);
#6578=SHAPE_REPRESENTATION('',(#4209),#6461);
#6580=PRODUCT_DEFINITION_CONTEXT('part definition',#6642,'design');
#6599=PRODUCT_DEFINITION('Flat Washer - M6','Flat Washer - M6',#6619,#6580);
#6619=PRODUCT_DEFINITION_FORMATION('',$,#6662);
#6642=APPLICATION_CONTEXT(
'Core Data for Automotive Mechanical Design Process');
#6643=PRODUCT_CONTEXT('part definition',#6642,'mechanical');
#6662=PRODUCT('Flat Washer - M6','Flat Washer - M6','Flat Washer - M6',
(#6643));
#6741=COLOUR_RGB('Black',0.12,0.14,0.17);
#6742=FILL_AREA_STYLE_COLOUR('',#6741);
#6743=FILL_AREA_STYLE('',(#6742));
#6744=SURFACE_STYLE_FILL_AREA(#6743);
#6745=SURFACE_SIDE_STYLE('',(#6744));
#6746=SURFACE_STYLE_USAGE(.BOTH.,#6745);
#6747=PRESENTATION_STYLE_ASSIGNMENT((#6746));
ENDSEC;
END-ISO-10303-21;
